ISO-10303-21;
HEADER;
FILE_DESCRIPTION (('STEP AP214'),
    '1' );
FILE_NAME ('Roller 2.step',
    '2026-10-26T17:37:43',
    ( '' ),
    ( '' ),
    'SwSTEP 2.0',
    'SolidWorks 2024',
    '' );
FILE_SCHEMA (( 'AUTOMOTIVE_DESIGN' ));
ENDSEC;

DATA;
#6=CARTESIAN_POINT ( 'NONE',  ( 12.69999999999999929, -3585.971999999999753, 2263.117139999999836 ) ) ;
#23=DIRECTION ( 'NONE',  ( 0.000000000000000000, 0.000000000000000000, -1.000000000000000000 ) ) ;
#26=CARTESIAN_POINT ( 'NONE',  ( 11.76763247656000111, -3642.196447741000156, 2279.779831143999672 ) ) ;
#80=DIRECTION ( 'NONE',  ( 0.000000000000000000, 0.000000000000000000, 1.000000000000000000 ) ) ;
#88=ORIENTED_EDGE ( 'NONE', *, *, #6716, .T. ) ;
#190=ORIENTED_EDGE ( 'NONE', *, *, #21850, .F. ) ;
#192=EDGE_LOOP ( 'NONE', ( #13601, #391, #20890, #19127 ) ) ;
#227=CARTESIAN_POINT ( 'NONE',  ( 9.855201422231997910, -3639.397391705999780, 2279.447341858000073 ) ) ;
#231=DIRECTION ( 'NONE',  ( 0.000000000000000000, 0.000000000000000000, -1.000000000000000000 ) ) ;
#256=ORIENTED_EDGE ( 'NONE', *, *, #14397, .F. ) ;
#258=CARTESIAN_POINT ( 'NONE',  ( 15.39424581079000021, -3598.565999368000121, 2279.486256121999759 ) ) ;
#320=ORIENTED_EDGE ( 'NONE', *, *, #15713, .T. ) ;
#334=CARTESIAN_POINT ( 'NONE',  ( 12.69997783158000004, -3636.657698770999559, 2279.817639764999967 ) ) ;
#350=CARTESIAN_POINT ( 'NONE',  ( 15.39424449907000003, -3640.434004351000112, 2279.486256451000372 ) ) ;
#367=EDGE_CURVE ( 'NONE', #20138, #17884, #3501, .T. ) ;
#378=DIRECTION ( 'NONE',  ( 1.000000000000000000, -0.000000000000000000, 1.224646799147353207E-16 ) ) ;
#391=ORIENTED_EDGE ( 'NONE', *, *, #20683, .T. ) ;
#432=EDGE_LOOP ( 'NONE', ( #3093, #2763, #22698, #4638, #1822, #2216, #11281, #2261, #21042, #12609, #19289, #12841, #4089, #6399 ) ) ;
#462=CARTESIAN_POINT ( 'NONE',  ( 15.27310817925000030, -3640.729796071000237, 2279.515941249000207 ) ) ;
#479=CARTESIAN_POINT ( 'NONE',  ( 9.855201422231997910, -3599.392391706000126, 2279.447341858000073 ) ) ;
#527=DIRECTION ( 'NONE',  ( 0.000000000000000000, -1.000000000000000000, 0.000000000000000000 ) ) ;
#535=DIRECTION ( 'NONE',  ( 0.000000000000000000, 0.000000000000000000, 1.000000000000000000 ) ) ;
#564=CARTESIAN_POINT ( 'NONE',  ( 9.855199999999999960, -3639.502500000000055, 2263.571799999999712 ) ) ;
#574=FACE_OUTER_BOUND ( 'NONE', #9837, .T. ) ;
#575=AXIS2_PLACEMENT_3D ( 'NONE', #15230, #18852, #11820 ) ;
#590=CARTESIAN_POINT ( 'NONE',  ( 15.48106175502000070, -3598.871388315999866, 2279.464089773000069 ) ) ;
#635=AXIS2_PLACEMENT_3D ( 'NONE', #7672, #12951, #21744 ) ;
#702=CARTESIAN_POINT ( 'NONE',  ( 14.71622495092000094, -3597.481870621000326, 2279.634028774999933 ) ) ;
#819=VERTEX_POINT ( 'NONE', #8838 ) ;
#824=CARTESIAN_POINT ( 'NONE',  ( 12.69999245750678263, -3602.342301254329868, 2279.817638608992183 ) ) ;
#853=DIRECTION ( 'NONE',  ( 1.000000000000000000, -3.122111992759158343E-13, 0.000000000000000000 ) ) ;
#865=CARTESIAN_POINT ( 'NONE',  ( 9.919062418924999847, -3600.124156707000111, 2279.464122714000041 ) ) ;
#892=CARTESIAN_POINT ( 'NONE',  ( 10.28147353980999945, -3597.988101833999735, 2279.551731614000346 ) ) ;
#925=VECTOR ( 'NONE', #12325, 1000.000000000000000 ) ;
#957=VERTEX_POINT ( 'NONE', #11176 ) ;
#986=CARTESIAN_POINT ( 'NONE',  ( 11.18998458582999866, -3601.915631438000219, 2279.715722610000284 ) ) ;
#1014=CARTESIAN_POINT ( 'NONE',  ( 11.18976463363000029, -3597.079503524999836, 2279.715692703000059 ) ) ;
#1021=ORIENTED_EDGE ( 'NONE', *, *, #18156, .F. ) ;
#1041=ORIENTED_EDGE ( 'NONE', *, *, #18117, .T. ) ;
#1066=ADVANCED_FACE ( 'NONE', ( #11734 ), #9746, .T. ) ;
#1094=PLANE ( 'NONE',  #3530 ) ;
#1096=CARTESIAN_POINT ( 'NONE',  ( 10.46820691843999995, -3601.271459550000145, 2279.591867610000008 ) ) ;
#1188=CARTESIAN_POINT ( 'NONE',  ( 12.70000000000085194, -3602.342301254449922, 2279.817638608976267 ) ) ;
#1236=EDGE_CURVE ( 'NONE', #3458, #17328, #6429, .T. ) ;
#1355=CARTESIAN_POINT ( 'NONE',  ( 12.69999999999999929, -3653.027999999999793, 2268.705139999999574 ) ) ;
#1375=AXIS2_PLACEMENT_3D ( 'NONE', #6437, #18969, #20843 ) ;
#1380=CIRCLE ( 'NONE', #12246, 5.587999999999926359 ) ;
#1386=CARTESIAN_POINT ( 'NONE',  ( 12.69999999999999929, -3648.710000000000036, 2257.592639999999847 ) ) ;
#1431=CARTESIAN_POINT ( 'NONE',  ( 12.69999245750621775, -3642.347301254329977, 2279.817638608992638 ) ) ;
#1526=CARTESIAN_POINT ( 'NONE',  ( 12.70000000000000107, -3590.289999999999964, 2279.817639999999756 ) ) ;
#1544=CARTESIAN_POINT ( 'NONE',  ( 15.54479999999999862, -3599.497499999999945, 2279.447335734999797 ) ) ;
#1648=CARTESIAN_POINT ( 'NONE',  ( 12.69999999999999929, -3590.289999999999964, 2268.705139999999574 ) ) ;
#1666=DIRECTION ( 'NONE',  ( 0.000000000000000000, -1.000000000000000000, 0.000000000000000000 ) ) ;
#1680=CARTESIAN_POINT ( 'NONE',  ( 12.69999999999999929, -3585.210000000000036, 2275.055139999999483 ) ) ;
#1772=AXIS2_PLACEMENT_3D ( 'NONE', #7987, #378, #20072 ) ;
#1781=DIRECTION ( 'NONE',  ( 0.000000000000000000, -1.000000000000000000, 0.000000000000000000 ) ) ;
#1798=CARTESIAN_POINT ( 'NONE',  ( 12.69999999999999929, -3653.027999999999793, 2268.705139999999574 ) ) ;
#1822=ORIENTED_EDGE ( 'NONE', *, *, #15713, .F. ) ;
#1824=CARTESIAN_POINT ( 'NONE',  ( 12.69999999999999929, -3648.710000000000036, 2268.705139999999574 ) ) ;
#1860=VERTEX_POINT ( 'NONE', #18604 ) ;
#1891=CARTESIAN_POINT ( 'NONE',  ( 12.69997737250858982, -3642.347301253999831, 2279.817639304488239 ) ) ;
#1963=DIRECTION ( 'NONE',  ( 0.000000000000000000, 1.000000000000000000, 0.000000000000000000 ) ) ;
#1970=TOROIDAL_SURFACE ( 'NONE', #16185, 5.588000000000000078, 0.7620000000000000107 ) ;
#1979=CARTESIAN_POINT ( 'NONE',  ( 10.28147353980999945, -3637.993101834000299, 2279.551731614000346 ) ) ;
#2073=CARTESIAN_POINT ( 'NONE',  ( 12.69999999999999929, -3653.789999999999964, 2268.705139999999574 ) ) ;
#2081=ORIENTED_EDGE ( 'NONE', *, *, #18439, .T. ) ;
#2101=CARTESIAN_POINT ( 'NONE',  ( 12.38520902594999917, -3636.669321837000098, 2279.814656244000162 ) ) ;
#2122=AXIS2_PLACEMENT_3D ( 'NONE', #20201, #18891, #8126 ) ;
#2159=CARTESIAN_POINT ( 'NONE',  ( 9.855201422231997910, -3599.497499926000273, 2279.447341858000073 ) ) ;
#2188=DIRECTION ( 'NONE',  ( 1.000000000000000000, 0.000000000000000000, 0.000000000000000000 ) ) ;
#2216=ORIENTED_EDGE ( 'NONE', *, *, #14685, .T. ) ;
#2243=CARTESIAN_POINT ( 'NONE',  ( 12.38520902594999917, -3596.664321836999989, 2279.814656244000162 ) ) ;
#2253=CARTESIAN_POINT ( 'NONE',  ( 12.69997737251000025, -3602.342301254000176, 2279.817638609000369 ) ) ;
#2257=( GEOMETRIC_REPRESENTATION_CONTEXT ( 3 ) GLOBAL_UNCERTAINTY_ASSIGNED_CONTEXT ( ( #16741 ) ) GLOBAL_UNIT_ASSIGNED_CONTEXT ( ( #21126, #3419, #23094 ) ) REPRESENTATION_CONTEXT ( 'NONE', 'WORKASPACE' ) );
#2261=ORIENTED_EDGE ( 'NONE', *, *, #20057, .T. ) ;
#2292=DIRECTION ( 'NONE',  ( 0.000000000000000000, 1.000000000000000000, 0.000000000000000000 ) ) ;
#2310=VECTOR ( 'NONE', #22317, 1000.000000000000000 ) ;
#2352=CARTESIAN_POINT ( 'NONE',  ( 13.63269713621999912, -3596.803664902999571, 2279.779803621000156 ) ) ;
#2456=CARTESIAN_POINT ( 'NONE',  ( 13.63269303062000048, -3642.196336588000122, 2279.779804022999997 ) ) ;
#2527=CARTESIAN_POINT ( 'NONE',  ( 12.38525565295999975, -3602.330681407000156, 2279.814657614000225 ) ) ;
#2535=PLANE ( 'NONE',  #12774 ) ;
#2606=CARTESIAN_POINT ( 'NONE',  ( 0.000000000000000000, 0.000000000000000000, 0.000000000000000000 ) ) ;
#2608=PRODUCT_DEFINITION_FORMATION_WITH_SPECIFIED_SOURCE ( 'ANY', '', #12377, .NOT_KNOWN. ) ;
#2643=EDGE_CURVE ( 'NONE', #22051, #18291, #17688, .T. ) ;
#2645=VERTEX_POINT ( 'NONE', #17940 ) ;
#2665=CYLINDRICAL_SURFACE ( 'NONE', #12066, 11.11249999999985860 ) ;
#2682=B_SPLINE_CURVE_WITH_KNOTS ( 'NONE', 3,
 ( #10336, #1431, #10099, #4826 ),
 .UNSPECIFIED., .F., .F.,
 ( 4, 4 ),
 ( 0.9999948892528710553, 1.000000000000000000 ),
 .UNSPECIFIED. ) ;
#2684=VERTEX_POINT ( 'NONE', #18292 ) ;
#2690=CARTESIAN_POINT ( 'NONE',  ( 12.69999999999999929, -3585.210000000000036, 2274.293139999999767 ) ) ;
#2727=DIRECTION ( 'NONE',  ( 1.000000000000000000, 0.000000000000000000, 0.000000000000000000 ) ) ;
#2743=DIRECTION ( 'NONE',  ( 0.000000000000000000, 1.000000000000000000, 0.000000000000000000 ) ) ;
#2745=DIRECTION ( 'NONE',  ( -1.000000000000000000, 0.000000000000000000, 0.000000000000000000 ) ) ;
#2763=ORIENTED_EDGE ( 'NONE', *, *, #2643, .F. ) ;
#2771=CARTESIAN_POINT ( 'NONE',  ( 13.92841025336000094, -3636.929928188000304, 2279.750815200000034 ) ) ;
#2780=VERTEX_POINT ( 'NONE', #2690 ) ;
#2805=AXIS2_PLACEMENT_3D ( 'NONE', #1824, #527, #13066 ) ;
#2868=CARTESIAN_POINT ( 'NONE',  ( 9.855201422231997910, -3599.497499926000273, 2279.447341858000073 ) ) ;
#2877=APPLICATION_CONTEXT ( 'configuration controlled 3d designs of mechanical parts and assemblies' ) ;
#2879=DIRECTION ( 'NONE',  ( 0.000000000000000000, -1.000000000000000000, 0.000000000000000000 ) ) ;
#2898=CARTESIAN_POINT ( 'NONE',  ( 10.12686798322000215, -3598.270251158000065, 2279.515935650000301 ) ) ;
#2989=DIRECTION ( 'NONE',  ( 0.000000000000000000, -1.000000000000000000, 0.000000000000000000 ) ) ;
#3027=ORIENTED_EDGE ( 'NONE', *, *, #14685, .F. ) ;
#3057=VERTEX_POINT ( 'NONE', #12305 ) ;
#3069=CARTESIAN_POINT ( 'NONE',  ( 13.63269303062000048, -3602.191336588000013, 2279.779804022999997 ) ) ;
#3093=ORIENTED_EDGE ( 'NONE', *, *, #5936, .F. ) ;
#3153=ORIENTED_EDGE ( 'NONE', *, *, #21141, .T. ) ;
#3170=AXIS2_PLACEMENT_3D ( 'NONE', #14577, #21719, #21836 ) ;
#3372=DIRECTION ( 'NONE',  ( 0.000000000000000000, 0.000000000000000000, -1.000000000000000000 ) ) ;
#3373=ORIENTED_EDGE ( 'NONE', *, *, #1236, .T. ) ;
#3381=EDGE_CURVE ( 'NONE', #2645, #17031, #13342, .T. ) ;
#3419=( NAMED_UNIT ( * ) PLANE_ANGLE_UNIT ( ) SI_UNIT ( $, .RADIAN. ) );
#3424=AXIS2_PLACEMENT_3D ( 'NONE', #8581, #10093, #13852 ) ;
#3426=FACE_BOUND ( 'NONE', #22361, .T. ) ;
#3431=ORIENTED_EDGE ( 'NONE', *, *, #7578, .F. ) ;
#3433=ORIENTED_EDGE ( 'NONE', *, *, #21311, .T. ) ;
#3458=VERTEX_POINT ( 'NONE', #17882 ) ;
#3490=EDGE_CURVE ( 'NONE', #12180, #2780, #1380, .T. ) ;
#3501=CIRCLE ( 'NONE', #20712, 6.349999999999855760 ) ;
#3524=CARTESIAN_POINT ( 'NONE',  ( 12.69999999999999929, -3653.027999999999793, 2268.705139999999574 ) ) ;
#3529=CARTESIAN_POINT ( 'NONE',  ( 9.855201422231997910, -3639.607849033000093, 2279.447341858000073 ) ) ;
#3530=AXIS2_PLACEMENT_3D ( 'NONE', #13526, #9774, #11758 ) ;
#3550=ADVANCED_FACE ( 'NONE', ( #10962 ), #9212, .F. ) ;
#3561=LINE ( 'NONE', #14239, #21212 ) ;
#3603=DIRECTION ( 'NONE',  ( 0.000000000000000000, -1.000000000000000000, 0.000000000000000000 ) ) ;
#3637=CIRCLE ( 'NONE', #1772, 0.7619999999999294005 ) ;
#3649=AXIS2_PLACEMENT_3D ( 'NONE', #18715, #13220, #7729 ) ;
#3650=CARTESIAN_POINT ( 'NONE',  ( 12.69999999999999929, -3590.289999999999964, 2268.705139999999574 ) ) ;
#3655=AXIS2_PLACEMENT_3D ( 'NONE', #13280, #4267, #13403 ) ;
#3722=CARTESIAN_POINT ( 'NONE',  ( 10.00572897464999933, -3638.571071898999890, 2279.486249620000308 ) ) ;
#3758=CARTESIAN_POINT ( 'NONE',  ( 10.12709285722000097, -3640.730217009000171, 2279.515989326000181 ) ) ;
#3814=EDGE_CURVE ( 'NONE', #3057, #15909, #6382, .T. ) ;
#3835=EDGE_CURVE ( 'NONE', #2645, #17044, #3637, .T. ) ;
#3844=CARTESIAN_POINT ( 'NONE',  ( 11.47173590547000011, -3636.929856508999819, 2279.750831905999803 ) ) ;
#3873=EDGE_LOOP ( 'NONE', ( #21688, #3433, #17455, #3027, #19839, #15558 ) ) ;
#3883=CARTESIAN_POINT ( 'NONE',  ( 10.00591156675000093, -3640.434449278999637, 2279.486295382999742 ) ) ;
#3905=AXIS2_PLACEMENT_3D ( 'NONE', #18230, #535, #2188 ) ;
#3979=CARTESIAN_POINT ( 'NONE',  ( 12.80540748638049386, -3642.347302934894742, 2279.817638395105860 ) ) ;
#4031=VECTOR ( 'NONE', #3603, 1000.000000000000000 ) ;
#4089=ORIENTED_EDGE ( 'NONE', *, *, #13868, .T. ) ;
#4132=ORIENTED_EDGE ( 'NONE', *, *, #15536, .F. ) ;
#4149=EDGE_CURVE ( 'NONE', #12180, #957, #20561, .T. ) ;
#4178=DIRECTION ( 'NONE',  ( 0.000000000000000000, -1.000000000000000000, 0.000000000000000000 ) ) ;
#4206=CARTESIAN_POINT ( 'NONE',  ( 15.54479999999999862, -3639.502500000000055, 2279.447335734999797 ) ) ;
#4221=AXIS2_PLACEMENT_3D ( 'NONE', #15392, #22521, #10109 ) ;
#4252=EDGE_LOOP ( 'NONE', ( #23082, #10266, #5772, #4132 ) ) ;
#4257=PLANE ( 'NONE',  #2122 ) ;
#4267=DIRECTION ( 'NONE',  ( 0.000000000000000000, 1.000000000000000000, 0.000000000000000000 ) ) ;
#4300=AXIS2_PLACEMENT_3D ( 'NONE', #4844, #12235, #19382 ) ;
#4308=CARTESIAN_POINT ( 'NONE',  ( 12.69999999999999929, -3590.289999999999964, 2275.055139999999483 ) ) ;
#4356=AXIS2_PLACEMENT_3D ( 'NONE', #2073, #10971, #80 ) ;
#4360=EDGE_CURVE ( 'NONE', #17332, #819, #7213, .T. ) ;
#4430=FACE_OUTER_BOUND ( 'NONE', #432, .T. ) ;
#4457=VERTEX_POINT ( 'NONE', #13813 ) ;
#4474=AXIS2_PLACEMENT_3D ( 'NONE', #6, #10429, #15940 ) ;
#4620=CARTESIAN_POINT ( 'NONE',  ( 10.68406120964000117, -3601.513414593999642, 2279.634081700000479 ) ) ;
#4638=ORIENTED_EDGE ( 'NONE', *, *, #20739, .F. ) ;
#4643=ORIENTED_EDGE ( 'NONE', *, *, #14715, .T. ) ;
#4714=DIRECTION ( 'NONE',  ( 0.000000000000000000, 1.000000000000000000, 0.000000000000000000 ) ) ;
#4735=DIRECTION ( 'NONE',  ( 0.000000000000000000, -1.000000000000000000, 0.000000000000000000 ) ) ;
#4743=EDGE_LOOP ( 'NONE', ( #5956, #1041 ) ) ;
#4744=DIRECTION ( 'NONE',  ( 0.000000000000000000, 0.000000000000000000, -1.000000000000000000 ) ) ;
#4757=ORIENTED_EDGE ( 'NONE', *, *, #9273, .T. ) ;
#4826=CARTESIAN_POINT ( 'NONE',  ( 12.69997737250858982, -3642.347301253999831, 2279.817639304488239 ) ) ;
#4844=CARTESIAN_POINT ( 'NONE',  ( 12.69999999999999929, -3585.971999999999753, 2274.293139999999767 ) ) ;
#4870=EDGE_LOOP ( 'NONE', ( #20910, #15089, #3153, #11415, #14519, #7147 ) ) ;
#4872=CIRCLE ( 'NONE', #10496, 11.11250000000000071 ) ;
#4954=DIRECTION ( 'NONE',  ( 0.000000000000000000, 0.000000000000000000, -1.000000000000000000 ) ) ;
#5076=FACE_OUTER_BOUND ( 'NONE', #20572, .T. ) ;
#5120=DIRECTION ( 'NONE',  ( 0.000000000000000000, 1.000000000000000000, 0.000000000000000000 ) ) ;
#5241=EDGE_CURVE ( 'NONE', #2780, #12180, #12224, .T. ) ;
#5359=AXIS2_PLACEMENT_3D ( 'NONE', #3650, #21813, #7407 ) ;
#5427=CARTESIAN_POINT ( 'NONE',  ( 12.69999999999999929, -3590.289999999999964, 2268.705139999999574 ) ) ;
#5507=CARTESIAN_POINT ( 'NONE',  ( 9.866773677518999364, -3639.188293979999798, 2279.450408114000311 ) ) ;
#5538=CARTESIAN_POINT ( 'NONE',  ( 15.54479999999999862, -3599.497499999999945, 2279.447335734999797 ) ) ;
#5547=CARTESIAN_POINT ( 'NONE',  ( 12.38525565295999975, -3642.335681406999811, 2279.814657614000225 ) ) ;
#5588=CARTESIAN_POINT ( 'NONE',  ( 12.69997932225824400, -3596.652698770999905, 2279.817639835496266 ) ) ;
#5611=AXIS2_PLACEMENT_3D ( 'NONE', #2606, #9751, #7545 ) ;
#5618=CARTESIAN_POINT ( 'NONE',  ( 10.92571717110000051, -3637.270967911999833, 2279.676081828000406 ) ) ;
#5632=CARTESIAN_POINT ( 'NONE',  ( 15.48106116729000092, -3640.128614708000441, 2279.464089926999804 ) ) ;
#5771=CARTESIAN_POINT ( 'NONE',  ( 11.47173590547000011, -3596.924856509000165, 2279.750831905999803 ) ) ;
#5772=ORIENTED_EDGE ( 'NONE', *, *, #1236, .F. ) ;
#5789=VERTEX_POINT ( 'NONE', #8546 ) ;
#5837=ADVANCED_FACE ( 'NONE', ( #22467 ), #13696, .T. ) ;
#5869=CARTESIAN_POINT ( 'NONE',  ( 15.54479999999999862, -3639.607668064999416, 2279.447335734999797 ) ) ;
#5910=ORIENTED_EDGE ( 'NONE', *, *, #22158, .T. ) ;
#5936=EDGE_CURVE ( 'NONE', #18291, #5789, #19787, .T. ) ;
#5956=ORIENTED_EDGE ( 'NONE', *, *, #17010, .T. ) ;
#5988=CARTESIAN_POINT ( 'NONE',  ( 12.70000000000000462, -3596.652698770568804, 2279.817639764978139 ) ) ;
#6052=CARTESIAN_POINT ( 'NONE',  ( 10.92596159350999940, -3601.729223875000116, 2279.676121195000178 ) ) ;
#6077=DIRECTION ( 'NONE',  ( 0.000000000000000000, 0.000000000000000000, 1.000000000000000000 ) ) ;
#6146=CYLINDRICAL_SURFACE ( 'NONE', #18074, 2.844799999999999773 ) ;
#6162=CARTESIAN_POINT ( 'NONE',  ( 11.47192027633000144, -3602.070229274999747, 2279.750852048000070 ) ) ;
#6192=CARTESIAN_POINT ( 'NONE',  ( 14.71622495092000094, -3637.486870620999980, 2279.634028774999933 ) ) ;
#6209=MANIFOLD_SOLID_BREP ( 'SOLID45-10[1]', #19962 ) ;
#6246=AXIS2_PLACEMENT_3D ( 'NONE', #6765, #12027, #10615 ) ;
#6265=CARTESIAN_POINT ( 'NONE',  ( 9.855201422231997910, -3639.502499925999928, 2279.447341858000073 ) ) ;
#6282=FACE_OUTER_BOUND ( 'NONE', #20277, .T. ) ;
#6382=B_SPLINE_CURVE_WITH_KNOTS ( 'NONE', 3,
 ( #12912, #824, #18642, #2253 ),
 .UNSPECIFIED., .F., .F.,
 ( 4, 4 ),
 ( 0.9999948892526789868, 1.000000000000000000 ),
 .UNSPECIFIED. ) ;
#6396=DIRECTION ( 'NONE',  ( 0.000000000000000000, 0.000000000000000000, 1.000000000000000000 ) ) ;
#6399=ORIENTED_EDGE ( 'NONE', *, *, #19154, .T. ) ;
#6404=DIRECTION ( 'NONE',  ( 0.000000000000000000, -1.000000000000000000, 0.000000000000000000 ) ) ;
#6429=CIRCLE ( 'NONE', #3424, 6.349999999999855760 ) ;
#6437=CARTESIAN_POINT ( 'NONE',  ( 12.69999999999999929, -3653.789999999999964, 2268.705139999999574 ) ) ;
#6485=CARTESIAN_POINT ( 'NONE',  ( 13.92840658401000020, -3602.070073557999876, 2279.750815596999928 ) ) ;
#6509=CARTESIAN_POINT ( 'NONE',  ( 12.69999999999999929, -3599.497499999999945, 2263.571799999999712 ) ) ;
#6528=EDGE_LOOP ( 'NONE', ( #11109, #10813, #20302, #11801 ) ) ;
#6539=CARTESIAN_POINT ( 'NONE',  ( 15.39424581079000021, -3638.570999367999775, 2279.486256121999759 ) ) ;
#6595=CARTESIAN_POINT ( 'NONE',  ( 12.69998522105610483, -3596.652698770827556, 2279.817639764999967 ) ) ;
#6609=CARTESIAN_POINT ( 'NONE',  ( 14.21033034659000016, -3601.915435226000227, 2279.715679318999719 ) ) ;
#6679=ADVANCED_FACE ( 'NONE', ( #6848 ), #10343, .T. ) ;
#6716=EDGE_CURVE ( 'NONE', #12318, #12735, #6731, .T. ) ;
#6731=LINE ( 'NONE', #7079, #14479 ) ;
#6763=DIRECTION ( 'NONE',  ( 0.000000000000000000, 1.000000000000000000, 0.000000000000000000 ) ) ;
#6765=CARTESIAN_POINT ( 'NONE',  ( 12.69999999999999929, -3653.789999999999964, 2268.705139999999574 ) ) ;
#6817=CARTESIAN_POINT ( 'NONE',  ( 9.855199999999999960, -3599.497499999999945, 2263.571799999999712 ) ) ;
#6848=FACE_OUTER_BOUND ( 'NONE', #11702, .T. ) ;
#6971=LINE ( 'NONE', #1680, #20812 ) ;
#6975=AXIS2_PLACEMENT_3D ( 'NONE', #6509, #20667, #20790 ) ;
#7048=CIRCLE ( 'NONE', #20883, 6.349999999999855760 ) ;
#7061=AXIS2_PLACEMENT_3D ( 'NONE', #21133, #19605, #4954 ) ;
#7079=CARTESIAN_POINT ( 'NONE',  ( 15.54479999999999862, -3599.497499999999945, 2263.571799999999712 ) ) ;
#7085=ORIENTED_EDGE ( 'NONE', *, *, #20679, .T. ) ;
#7147=ORIENTED_EDGE ( 'NONE', *, *, #20057, .F. ) ;
#7174=VERTEX_POINT ( 'NONE', #12490 ) ;
#7180=SHAPE_DEFINITION_REPRESENTATION ( #10697, #13400 ) ;
#7213=B_SPLINE_CURVE_WITH_KNOTS ( 'NONE', 3,
 ( #4206, #5869, #18497, #5632, #350, #462, #7491, #14651, #12885, #22013, #14884, #14990, #2456, #9707, #9483, #3979, #7842 ),
 .UNSPECIFIED., .F., .F.,
 ( 4, 1, 1, 1, 1, 1, 1, 1, 1, 1, 1, 1, 1, 1, 4 ),
 ( 0.000000000000000000, 0.07142857142856999519, 0.1428571428570999946, 0.2142857142857000075, 0.2857142857143000203, 0.3571428571429000054, 0.4285714285713999594, 0.5000000000000000000, 0.5714285714286000406, 0.6428571428570999391, 0.7142857142856999797, 0.7857142857142999093, 0.8571428571429000609, 0.9285714285714000704, 0.9999948892528710553 ),
 .UNSPECIFIED. ) ;
#7291=( NAMED_UNIT ( * ) SI_UNIT ( $, .STERADIAN. ) SOLID_ANGLE_UNIT ( ) );
#7322=LINE ( 'NONE', #11058, #7603 ) ;
#7407=DIRECTION ( 'NONE',  ( 1.000000000000000000, 0.000000000000000000, 3.996303350731721563E-14 ) ) ;
#7412=PRODUCT_CONTEXT ( 'NONE', #2877, 'mechanical' ) ;
#7491=CARTESIAN_POINT ( 'NONE',  ( 15.11851036462000053, -3641.011922182000035, 2279.551735152999754 ) ) ;
#7545=DIRECTION ( 'NONE',  ( 1.000000000000000000, 0.000000000000000000, 0.000000000000000000 ) ) ;
#7578=EDGE_CURVE ( 'NONE', #18291, #22051, #4872, .T. ) ;
#7587=EDGE_LOOP ( 'NONE', ( #3431, #21047, #19798, #4643, #7991, #20153, #8641, #320, #17586, #17699 ) ) ;
#7594=LINE ( 'NONE', #564, #20054 ) ;
#7603=VECTOR ( 'NONE', #8963, 1000.000000000000000 ) ;
#7616=CARTESIAN_POINT ( 'NONE',  ( 13.32717689757000024, -3596.716669530999752, 2279.801370455999859 ) ) ;
#7636=EDGE_CURVE ( 'NONE', #20355, #15900, #18490, .T. ) ;
#7672=CARTESIAN_POINT ( 'NONE',  ( 12.69999999999999929, -3653.789999999999964, 2268.705139999999574 ) ) ;
#7729=DIRECTION ( 'NONE',  ( 1.000000000000000000, 0.000000000000000000, 0.000000000000000000 ) ) ;
#7787=CARTESIAN_POINT ( 'NONE',  ( 12.69999999999999929, -3653.789999999999964, 2274.293139999999767 ) ) ;
#7828=ORIENTED_EDGE ( 'NONE', *, *, #11880, .F. ) ;
#7842=CARTESIAN_POINT ( 'NONE',  ( 12.69999999999999929, -3642.347301254450485, 2279.817638608977632 ) ) ;
#7854=CARTESIAN_POINT ( 'NONE',  ( 15.27310946263999902, -3598.270206608000080, 2279.515940941999816 ) ) ;
#7887=DIRECTION ( 'NONE',  ( 0.000000000000000000, -1.000000000000000000, 0.000000000000000000 ) ) ;
#7987=CARTESIAN_POINT ( 'NONE',  ( 12.69999999999999929, -3653.027999999999793, 2263.117139999999836 ) ) ;
#7991=ORIENTED_EDGE ( 'NONE', *, *, #16735, .T. ) ;
#8030=CARTESIAN_POINT ( 'NONE',  ( 10.28172140950000113, -3601.007291280000118, 2279.551786969999739 ) ) ;
#8033=AXIS2_PLACEMENT_3D ( 'NONE', #22787, #6763, #20932 ) ;
#8083=B_SPLINE_CURVE_WITH_KNOTS ( 'NONE', 3,
 ( #21551, #227, #5507, #12642, #3722, #10880, #1979, #9128, #16271, #5618, #12870, #3844, #10995, #18137, #2101, #9243, #334 ),
 .UNSPECIFIED., .F., .F.,
 ( 4, 1, 1, 1, 1, 1, 1, 1, 1, 1, 1, 1, 1, 1, 4 ),
 ( 0.000000000000000000, 0.07142857142856999519, 0.1428571428570999946, 0.2142857142857000075, 0.2857142857143000203, 0.3571428571429000054, 0.4285714285713999594, 0.5000000000000000000, 0.5714285714286000406, 0.6428571428570999391, 0.7142857142856999797, 0.7857142857142999093, 0.8571428571429000609, 0.9285714285714000704, 1.000000000000000000 ),
 .UNSPECIFIED. ) ;
#8126=DIRECTION ( 'NONE',  ( 0.000000000000000000, 0.000000000000000000, -1.000000000000000000 ) ) ;
#8150=CYLINDRICAL_SURFACE ( 'NONE', #6975, 2.844799999999999773 ) ;
#8195=CYLINDRICAL_SURFACE ( 'NONE', #575, 11.11249999999985860 ) ;
#8287=CARTESIAN_POINT ( 'NONE',  ( 15.54479999999999862, -3639.397331916999974, 2279.447335734999797 ) ) ;
#8409=CARTESIAN_POINT ( 'NONE',  ( 10.00572897464999933, -3598.566071899000235, 2279.486249620000308 ) ) ;
#8421=CIRCLE ( 'NONE', #3170, 11.11250000000000071 ) ;
#8449=CIRCLE ( 'NONE', #21547, 6.349999999999855760 ) ;
#8464=ORIENTED_EDGE ( 'NONE', *, *, #6716, .F. ) ;
#8476=CIRCLE ( 'NONE', #4300, 0.7619999999999294005 ) ;
#8520=DIRECTION ( 'NONE',  ( 0.000000000000000000, 0.000000000000000000, 1.000000000000000000 ) ) ;
#8540=CARTESIAN_POINT ( 'NONE',  ( 12.69999261053000872, -3636.657698770683055, 2279.817639764992691 ) ) ;
#8546=CARTESIAN_POINT ( 'NONE',  ( 12.70000000000000462, -3596.652698770568804, 2279.817639764978139 ) ) ;
#8581=CARTESIAN_POINT ( 'NONE',  ( 12.69999999999999929, -3648.710000000000036, 2268.705139999999574 ) ) ;
#8604=B_SPLINE_CURVE_WITH_KNOTS ( 'NONE', 3,
 ( #18797, #16920, #2527, #22537, #20449, #6162, #986, #6052, #4620, #1096, #8030, #15292, #13416, #865, #11759, #18682, #2868 ),
 .UNSPECIFIED., .F., .F.,
 ( 4, 1, 1, 1, 1, 1, 1, 1, 1, 1, 1, 1, 1, 1, 4 ),
 ( 0.000000000000000000, 0.07142857142856999519, 0.1428571428570999946, 0.2142857142857000075, 0.2857142857143000203, 0.3571428571429000054, 0.4285714285713999594, 0.5000000000000000000, 0.5714285714286000406, 0.6428571428570999391, 0.7142857142856999797, 0.7857142857142999093, 0.8571428571429000609, 0.9285714285714000704, 1.000000000000000000 ),
 .UNSPECIFIED. ) ;
#8627=DIRECTION ( 'NONE',  ( 0.000000000000000000, 0.000000000000000000, 1.000000000000000000 ) ) ;
#8641=ORIENTED_EDGE ( 'NONE', *, *, #4360, .T. ) ;
#8658=ORIENTED_EDGE ( 'NONE', *, *, #3381, .F. ) ;
#8665=VECTOR ( 'NONE', #2989, 1000.000000000000000 ) ;
#8702=CARTESIAN_POINT ( 'NONE',  ( 15.54479999999999862, -3599.602668064999762, 2279.447335734999797 ) ) ;
#8731=VERTEX_POINT ( 'NONE', #20070 ) ;
#8774=ORIENTED_EDGE ( 'NONE', *, *, #14188, .F. ) ;
#8806=DIRECTION ( 'NONE',  ( 0.000000000000000000, 0.000000000000000000, -1.000000000000000000 ) ) ;
#8822=DIRECTION ( 'NONE',  ( 0.000000000000000000, 0.000000000000000000, -1.000000000000000000 ) ) ;
#8838=CARTESIAN_POINT ( 'NONE',  ( 12.69999999999999929, -3642.347301254450485, 2279.817638608977632 ) ) ;
#8845=AXIS2_PLACEMENT_3D ( 'NONE', #10599, #17740, #4744 ) ;
#8963=DIRECTION ( 'NONE',  ( 0.000000000000000000, -1.000000000000000000, 0.000000000000000000 ) ) ;
#9044=CARTESIAN_POINT ( 'NONE',  ( 11.18998458582999866, -3641.920631437999873, 2279.715722610000284 ) ) ;
#9085=EDGE_LOOP ( 'NONE', ( #19917, #15981 ) ) ;
#9094=ADVANCED_BREP_SHAPE_REPRESENTATION ( '', ( #6209, #5611 ), #11980 ) ;
#9128=CARTESIAN_POINT ( 'NONE',  ( 10.46794630892000022, -3637.728865433999999, 2279.591814147000150 ) ) ;
#9164=ADVANCED_FACE ( 'NONE', ( #574 ), #11130, .F. ) ;
#9212=PLANE ( 'NONE',  #635 ) ;
#9233=CARTESIAN_POINT ( 'NONE',  ( 12.69999999999999929, -3585.971999999999753, 2268.705139999999574 ) ) ;
#9243=CARTESIAN_POINT ( 'NONE',  ( 12.59468037889999970, -3636.657701233000353, 2279.817639764999967 ) ) ;
#9247=EDGE_CURVE ( 'NONE', #8731, #21632, #16908, .T. ) ;
#9273=EDGE_CURVE ( 'NONE', #957, #17291, #7048, .T. ) ;
#9391=CARTESIAN_POINT ( 'NONE',  ( 10.46794630892000022, -3597.723865433999890, 2279.591814147000150 ) ) ;
#9410=ORIENTED_EDGE ( 'NONE', *, *, #9273, .F. ) ;
#9483=CARTESIAN_POINT ( 'NONE',  ( 13.01510455369313490, -3642.335645362285504, 2279.814648973302610 ) ) ;
#9555=FACE_OUTER_BOUND ( 'NONE', #18340, .T. ) ;
#9630=CARTESIAN_POINT ( 'NONE',  ( 12.69999999999999929, -3585.971999999999753, 2275.055139999999483 ) ) ;
#9632=ORIENTED_EDGE ( 'NONE', *, *, #14397, .T. ) ;
#9661=ADVANCED_FACE ( 'NONE', ( #5076 ), #15630, .T. ) ;
#9694=CARTESIAN_POINT ( 'NONE',  ( 15.11851230223999920, -3637.993080951000593, 2279.551734718999796 ) ) ;
#9707=CARTESIAN_POINT ( 'NONE',  ( 13.32717070831999884, -3642.283331859000100, 2279.801370659999975 ) ) ;
#9716=FACE_OUTER_BOUND ( 'NONE', #7587, .T. ) ;
#9746=CYLINDRICAL_SURFACE ( 'NONE', #9769, 6.349999999999855760 ) ;
#9751=DIRECTION ( 'NONE',  ( 0.000000000000000000, 0.000000000000000000, 1.000000000000000000 ) ) ;
#9769=AXIS2_PLACEMENT_3D ( 'NONE', #22392, #7887, #13389 ) ;
#9774=DIRECTION ( 'NONE',  ( 0.000000000000000000, 0.000000000000000000, -1.000000000000000000 ) ) ;
#9775=FACE_OUTER_BOUND ( 'NONE', #21417, .T. ) ;
#9803=CARTESIAN_POINT ( 'NONE',  ( 14.47434230490000040, -3637.271017030000166, 2279.676071933000003 ) ) ;
#9815=CIRCLE ( 'NONE', #4221, 0.7619999999999294005 ) ;
#9837=EDGE_LOOP ( 'NONE', ( #8774, #19104, #190, #11113, #18202, #8464 ) ) ;
#9887=DIRECTION ( 'NONE',  ( 0.000000000000000000, 0.000000000000000000, 1.000000000000000000 ) ) ;
#9914=CARTESIAN_POINT ( 'NONE',  ( 15.53320999718999929, -3639.188150532000236, 2279.450415100000100 ) ) ;
#9984=CARTESIAN_POINT ( 'NONE',  ( 12.69999999999999929, -3590.289999999999964, 2268.705139999999574 ) ) ;
#10011=PLANE ( 'NONE',  #20761 ) ;
#10018=DIRECTION ( 'NONE',  ( 1.000000000000000000, -3.122111992759158343E-13, 0.000000000000000000 ) ) ;
#10028=ORIENTED_EDGE ( 'NONE', *, *, #20683, .F. ) ;
#10039=CARTESIAN_POINT ( 'NONE',  ( 11.76748838596000013, -3596.803600169999754, 2279.779819357000179 ) ) ;
#10044=DIRECTION ( 'NONE',  ( 0.000000000000000000, -1.000000000000000000, 0.000000000000000000 ) ) ;
#10081=AXIS2_PLACEMENT_3D ( 'NONE', #10244, #2743, #9887 ) ;
#10093=DIRECTION ( 'NONE',  ( 0.000000000000000000, 1.000000000000000000, 0.000000000000000000 ) ) ;
#10099=CARTESIAN_POINT ( 'NONE',  ( 12.69998491500954962, -3642.347301254179911, 2279.817638609000369 ) ) ;
#10109=DIRECTION ( 'NONE',  ( 0.000000000000000000, 0.000000000000000000, 1.000000000000000000 ) ) ;
#10183=PRODUCT_DEFINITION_CONTEXT ( 'detailed design', #21162, 'design' ) ;
#10185=VECTOR ( 'NONE', #4178, 1000.000000000000000 ) ;
#10244=CARTESIAN_POINT ( 'NONE',  ( 12.69999999999999929, -3585.971999999999753, 2268.705139999999574 ) ) ;
#10266=ORIENTED_EDGE ( 'NONE', *, *, #10653, .T. ) ;
#10336=CARTESIAN_POINT ( 'NONE',  ( 12.69999999999999929, -3642.347301254450485, 2279.817638608977632 ) ) ;
#10343=TOROIDAL_SURFACE ( 'NONE', #18963, 5.588000000000000078, 0.7620000000000000107 ) ;
#10381=CARTESIAN_POINT ( 'NONE',  ( 12.69999999999999929, -3653.789999999999964, 2268.705139999999574 ) ) ;
#10400=CARTESIAN_POINT ( 'NONE',  ( 12.69997783158000004, -3636.657698770999559, 2279.817639764999967 ) ) ;
#10429=DIRECTION ( 'NONE',  ( -1.000000000000000000, -0.000000000000000000, -0.000000000000000000 ) ) ;
#10496=AXIS2_PLACEMENT_3D ( 'NONE', #9984, #4714, #11865 ) ;
#10525=ADVANCED_FACE ( 'NONE', ( #21154 ), #18936, .T. ) ;
#10527=CARTESIAN_POINT ( 'NONE',  ( 12.69999999999999929, -3590.289999999999964, 2268.705139999999574 ) ) ;
#10539=B_SPLINE_CURVE_WITH_KNOTS ( 'NONE', 3,
 ( #15208, #479, #17299, #20062, #8409, #2898, #892, #9391, #15555, #20829, #1014, #5771, #10039, #15438, #2243, #22449, #11148 ),
 .UNSPECIFIED., .F., .F.,
 ( 4, 1, 1, 1, 1, 1, 1, 1, 1, 1, 1, 1, 1, 1, 4 ),
 ( 0.000000000000000000, 0.07142857142856999519, 0.1428571428570999946, 0.2142857142857000075, 0.2857142857143000203, 0.3571428571429000054, 0.4285714285713999594, 0.5000000000000000000, 0.5714285714286000406, 0.6428571428570999391, 0.7142857142856999797, 0.7857142857142999093, 0.8571428571429000609, 0.9285714285714000704, 1.000000000000000000 ),
 .UNSPECIFIED. ) ;
#10580=FACE_OUTER_BOUND ( 'NONE', #12764, .T. ) ;
#10599=CARTESIAN_POINT ( 'NONE',  ( 12.69999999999999929, -3585.971999999999753, 2268.705139999999574 ) ) ;
#10615=DIRECTION ( 'NONE',  ( 0.000000000000000000, 0.000000000000000000, 1.000000000000000000 ) ) ;
#10653=EDGE_CURVE ( 'NONE', #17044, #17328, #3561, .T. ) ;
#10697=PRODUCT_DEFINITION_SHAPE ( 'NONE', 'NONE',  #22796 ) ;
#10795=ADVANCED_FACE ( 'NONE', ( #13498, #20316 ), #4257, .T. ) ;
#10813=ORIENTED_EDGE ( 'NONE', *, *, #18901, .F. ) ;
#10820=ORIENTED_EDGE ( 'NONE', *, *, #17147, .F. ) ;
#10880=CARTESIAN_POINT ( 'NONE',  ( 10.12686798322000215, -3638.275251157999719, 2279.515935650000301 ) ) ;
#10907=B_SPLINE_CURVE_WITH_KNOTS ( 'NONE', 3,
 ( #5588, #6595, #16690, #16574 ),
 .UNSPECIFIED., .F., .F.,
 ( 4, 4 ),
 ( 0.000000000000000000, 5.006989608022782729E-06 ),
 .UNSPECIFIED. ) ;
#10915=CARTESIAN_POINT ( 'NONE',  ( 9.866830068855998448, -3639.817301451999811, 2279.450423099000091 ) ) ;
#10962=FACE_OUTER_BOUND ( 'NONE', #12303, .T. ) ;
#10971=DIRECTION ( 'NONE',  ( 0.000000000000000000, 1.000000000000000000, 0.000000000000000000 ) ) ;
#10981=DIRECTION ( 'NONE',  ( 0.000000000000000000, 0.000000000000000000, 1.000000000000000000 ) ) ;
#10985=FACE_OUTER_BOUND ( 'NONE', #22538, .T. ) ;
#10995=CARTESIAN_POINT ( 'NONE',  ( 11.76748838596000013, -3636.808600170000318, 2279.779819357000179 ) ) ;
#10998=CIRCLE ( 'NONE', #22573, 2.844799999999999773 ) ;
#11058=CARTESIAN_POINT ( 'NONE',  ( 12.69999999999999929, -3585.210000000000036, 2262.355140000000119 ) ) ;
#11079=B_SPLINE_CURVE_WITH_KNOTS ( 'NONE', 3,
 ( #1544, #8702, #15496, #15848, #20894, #11978, #19131, #17245, #22979, #14095, #6609, #6485, #3069, #13622, #20768, #11866, #1188 ),
 .UNSPECIFIED., .F., .F.,
 ( 4, 1, 1, 1, 1, 1, 1, 1, 1, 1, 1, 1, 1, 1, 4 ),
 ( 0.000000000000000000, 0.07142857142856999519, 0.1428571428570999946, 0.2142857142857000075, 0.2857142857143000203, 0.3571428571429000054, 0.4285714285713999594, 0.5000000000000000000, 0.5714285714286000406, 0.6428571428570999391, 0.7142857142856999797, 0.7857142857142999093, 0.8571428571429000609, 0.9285714285714000704, 0.9999948892526789868 ),
 .UNSPECIFIED. ) ;
#11109=ORIENTED_EDGE ( 'NONE', *, *, #3835, .F. ) ;
#11113=ORIENTED_EDGE ( 'NONE', *, *, #3814, .F. ) ;
#11130=CYLINDRICAL_SURFACE ( 'NONE', #3649, 2.844799999999999773 ) ;
#11148=CARTESIAN_POINT ( 'NONE',  ( 12.69997932225824400, -3596.652698770999905, 2279.817639835496266 ) ) ;
#11172=ORIENTED_EDGE ( 'NONE', *, *, #13804, .F. ) ;
#11176=CARTESIAN_POINT ( 'NONE',  ( 12.69999999999999929, -3585.971999999999753, 2262.355140000000119 ) ) ;
#11252=CARTESIAN_POINT ( 'NONE',  ( 12.80540911176254859, -3596.652697124181941, 2279.817639555324604 ) ) ;
#11281=ORIENTED_EDGE ( 'NONE', *, *, #7636, .T. ) ;
#11415=ORIENTED_EDGE ( 'NONE', *, *, #21334, .F. ) ;
#11451=B_SPLINE_CURVE_WITH_KNOTS ( 'NONE', 3,
 ( #5988, #11252, #18396, #7616, #2352, #18511, #18167, #16632, #702, #21803, #12897, #7854, #258, #590, #22024, #21583, #5538 ),
 .UNSPECIFIED., .F., .F.,
 ( 4, 1, 1, 1, 1, 1, 1, 1, 1, 1, 1, 1, 1, 1, 4 ),
 ( 5.006989608022782729E-06, 0.07142857142856999519, 0.1428571428570999946, 0.2142857142857000075, 0.2857142857143000203, 0.3571428571429000054, 0.4285714285713999594, 0.5000000000000000000, 0.5714285714286000406, 0.6428571428570999391, 0.7142857142856999797, 0.7857142857142999093, 0.8571428571429000609, 0.9285714285714000704, 1.000000000000000000 ),
 .UNSPECIFIED. ) ;
#11541=LINE ( 'NONE', #20559, #2310 ) ;
#11603=CARTESIAN_POINT ( 'NONE',  ( 12.69999999999999929, -3648.710000000000036, 2262.355140000000119 ) ) ;
#11624=FACE_OUTER_BOUND ( 'NONE', #3873, .T. ) ;
#11702=EDGE_LOOP ( 'NONE', ( #8658, #12875, #5910, #10820 ) ) ;
#11734=FACE_OUTER_BOUND ( 'NONE', #18541, .T. ) ;
#11758=DIRECTION ( 'NONE',  ( 0.000000000000000000, -1.000000000000000000, 0.000000000000000000 ) ) ;
#11759=CARTESIAN_POINT ( 'NONE',  ( 9.866830068855998448, -3599.812301451999701, 2279.450423099000091 ) ) ;
#11796=CARTESIAN_POINT ( 'NONE',  ( 13.01510790209967894, -3636.669354860410749, 2279.814648369741917 ) ) ;
#11801=ORIENTED_EDGE ( 'NONE', *, *, #13804, .T. ) ;
#11820=DIRECTION ( 'NONE',  ( 0.000000000000000000, 0.000000000000000000, -1.000000000000000000 ) ) ;
#11829=ORIENTED_EDGE ( 'NONE', *, *, #14188, .T. ) ;
#11865=DIRECTION ( 'NONE',  ( 1.000000000000000000, 0.000000000000000000, 3.996303350731721563E-14 ) ) ;
#11866=CARTESIAN_POINT ( 'NONE',  ( 12.80540748638105697, -3602.342302934895088, 2279.817638395105860 ) ) ;
#11880=EDGE_CURVE ( 'NONE', #5789, #12735, #11451, .T. ) ;
#11916=CARTESIAN_POINT ( 'NONE',  ( 13.32717689757000024, -3636.721669530999861, 2279.801370455999859 ) ) ;
#11978=CARTESIAN_POINT ( 'NONE',  ( 15.27310817925000030, -3600.724796071000128, 2279.515941249000207 ) ) ;
#11980=( GEOMETRIC_REPRESENTATION_CONTEXT ( 3 ) GLOBAL_UNCERTAINTY_ASSIGNED_CONTEXT ( ( #20261 ) ) GLOBAL_UNIT_ASSIGNED_CONTEXT ( ( #17013, #12678, #7291 ) ) REPRESENTATION_CONTEXT ( 'NONE', 'WORKASPACE' ) );
#12027=DIRECTION ( 'NONE',  ( 0.000000000000000000, -1.000000000000000000, 0.000000000000000000 ) ) ;
#12066=AXIS2_PLACEMENT_3D ( 'NONE', #20948, #10044, #17538 ) ;
#12087=CARTESIAN_POINT ( 'NONE',  ( 15.54479999999999862, -3639.502500000000055, 2263.571799999999712 ) ) ;
#12127=CARTESIAN_POINT ( 'NONE',  ( 12.69999999999999929, -3585.210000000000036, 2268.705139999999574 ) ) ;
#12180=VERTEX_POINT ( 'NONE', #19674 ) ;
#12224=CIRCLE ( 'NONE', #3655, 5.587999999999926359 ) ;
#12235=DIRECTION ( 'NONE',  ( 1.000000000000000000, 0.000000000000000000, -1.224646799147353207E-16 ) ) ;
#12246=AXIS2_PLACEMENT_3D ( 'NONE', #19766, #2292, #14493 ) ;
#12303=EDGE_LOOP ( 'NONE', ( #15618, #13468 ) ) ;
#12305=CARTESIAN_POINT ( 'NONE',  ( 12.70000000000085194, -3602.342301254449922, 2279.817638608976267 ) ) ;
#12318=VERTEX_POINT ( 'NONE', #21890 ) ;
#12325=DIRECTION ( 'NONE',  ( 0.000000000000000000, 0.000000000000000000, 1.000000000000000000 ) ) ;
#12377=PRODUCT ( 'Roller 2', 'Roller 2', '', ( #7412 ) ) ;
#12416=DIRECTION ( 'NONE',  ( 0.000000000000000000, -1.000000000000000000, 0.000000000000000000 ) ) ;
#12463=ORIENTED_EDGE ( 'NONE', *, *, #3490, .T. ) ;
#12490=CARTESIAN_POINT ( 'NONE',  ( 15.54479999999999862, -3639.502500000000964, 2263.571799999999712 ) ) ;
#12520=AXIS2_PLACEMENT_3D ( 'NONE', #10381, #15894, #8627 ) ;
#12561=CARTESIAN_POINT ( 'NONE',  ( 10.92596159350999940, -3641.734223874999770, 2279.676121195000178 ) ) ;
#12609=ORIENTED_EDGE ( 'NONE', *, *, #16735, .F. ) ;
#12642=CARTESIAN_POINT ( 'NONE',  ( 9.918918857905000053, -3638.876466522000101, 2279.464085466000142 ) ) ;
#12677=CARTESIAN_POINT ( 'NONE',  ( 10.46820691843999995, -3641.276459549999799, 2279.591867610000008 ) ) ;
#12678=( NAMED_UNIT ( * ) PLANE_ANGLE_UNIT ( ) SI_UNIT ( $, .RADIAN. ) );
#12735=VERTEX_POINT ( 'NONE', #16244 ) ;
#12764=EDGE_LOOP ( 'NONE', ( #13704, #20163 ) ) ;
#12774=AXIS2_PLACEMENT_3D ( 'NONE', #12127, #2879, #21043 ) ;
#12841=ORIENTED_EDGE ( 'NONE', *, *, #21850, .T. ) ;
#12843=ADVANCED_FACE ( 'NONE', ( #16582 ), #16361, .F. ) ;
#12870=CARTESIAN_POINT ( 'NONE',  ( 11.18976463363000029, -3637.084503524999491, 2279.715692703000059 ) ) ;
#12874=CIRCLE ( 'NONE', #21492, 6.349999999999855760 ) ;
#12875=ORIENTED_EDGE ( 'NONE', *, *, #3835, .T. ) ;
#12885=CARTESIAN_POINT ( 'NONE',  ( 14.71622237244000075, -3641.518131980000362, 2279.634029254999859 ) ) ;
#12890=ADVANCED_FACE ( 'NONE', ( #6282 ), #1094, .F. ) ;
#12897=CARTESIAN_POINT ( 'NONE',  ( 15.11851230223999920, -3597.988080951000029, 2279.551734718999796 ) ) ;
#12912=CARTESIAN_POINT ( 'NONE',  ( 12.70000000000085194, -3602.342301254449922, 2279.817638608976267 ) ) ;
#12941=ORIENTED_EDGE ( 'NONE', *, *, #367, .T. ) ;
#12951=DIRECTION ( 'NONE',  ( -0.000000000000000000, 1.000000000000000000, 0.000000000000000000 ) ) ;
#13001=ADVANCED_FACE ( 'NONE', ( #15176 ), #10011, .F. ) ;
#13066=DIRECTION ( 'NONE',  ( 1.000000000000000000, 0.000000000000000000, 3.996303350731721563E-14 ) ) ;
#13071=DIRECTION ( 'NONE',  ( 0.000000000000000000, 0.000000000000000000, -1.000000000000000000 ) ) ;
#13167=CARTESIAN_POINT ( 'NONE',  ( 12.69999999999999929, -3639.502500000000055, 2263.571799999999712 ) ) ;
#13220=DIRECTION ( 'NONE',  ( 0.000000000000000000, 0.000000000000000000, 1.000000000000000000 ) ) ;
#13228=AXIS2_PLACEMENT_3D ( 'NONE', #15648, #17040, #2745 ) ;
#13280=CARTESIAN_POINT ( 'NONE',  ( 12.69999999999999929, -3585.210000000000036, 2268.705139999999574 ) ) ;
#13311=LINE ( 'NONE', #16818, #10185 ) ;
#13342=CIRCLE ( 'NONE', #6246, 5.587999999999926359 ) ;
#13389=DIRECTION ( 'NONE',  ( 0.000000000000000000, 0.000000000000000000, -1.000000000000000000 ) ) ;
#13400=SHAPE_REPRESENTATION ( 'Roller 2', ( #5611 ), #11980 ) ;
#13403=DIRECTION ( 'NONE',  ( 0.000000000000000000, 0.000000000000000000, -1.000000000000000000 ) ) ;
#13416=CARTESIAN_POINT ( 'NONE',  ( 10.00591156675000093, -3600.429449278999982, 2279.486295382999742 ) ) ;
#13468=ORIENTED_EDGE ( 'NONE', *, *, #3381, .T. ) ;
#13498=FACE_BOUND ( 'NONE', #17001, .T. ) ;
#13526=CARTESIAN_POINT ( 'NONE',  ( 12.69999999999999929, -3599.497499999999945, 2263.571799999999712 ) ) ;
#13558=CARTESIAN_POINT ( 'NONE',  ( 12.80540911176311170, -3636.657697124182050, 2279.817639555324149 ) ) ;
#13601=ORIENTED_EDGE ( 'NONE', *, *, #5241, .F. ) ;
#13607=CIRCLE ( 'NONE', #13228, 2.844799999999999773 ) ;
#13622=CARTESIAN_POINT ( 'NONE',  ( 13.32717070831999884, -3602.278331858999991, 2279.801370659999975 ) ) ;
#13696=CYLINDRICAL_SURFACE ( 'NONE', #1375, 6.349999999999855760 ) ;
#13704=ORIENTED_EDGE ( 'NONE', *, *, #2643, .T. ) ;
#13804=EDGE_CURVE ( 'NONE', #18172, #17044, #8449, .T. ) ;
#13813=CARTESIAN_POINT ( 'NONE',  ( 12.70000000000000107, -3648.710000000000036, 2279.817639999999756 ) ) ;
#13843=CARTESIAN_POINT ( 'NONE',  ( 12.69999999999999929, -3653.027999999999793, 2275.055139999999483 ) ) ;
#13852=DIRECTION ( 'NONE',  ( 0.000000000000000000, 0.000000000000000000, -1.000000000000000000 ) ) ;
#13868=EDGE_CURVE ( 'NONE', #20725, #16084, #10539, .T. ) ;
#13882=CARTESIAN_POINT ( 'NONE',  ( 12.69999999999999929, -3590.289999999999964, 2257.592639999999847 ) ) ;
#13956=DIRECTION ( 'NONE',  ( 0.000000000000000000, 0.000000000000000000, 1.000000000000000000 ) ) ;
#13989=DIRECTION ( 'NONE',  ( 0.000000000000000000, 1.000000000000000000, 0.000000000000000000 ) ) ;
#14095=CARTESIAN_POINT ( 'NONE',  ( 14.47433926966999884, -3601.728985385999749, 2279.676072425999791 ) ) ;
#14127=CARTESIAN_POINT ( 'NONE',  ( 12.69999999999999929, -3599.497499999999945, 2263.571799999999712 ) ) ;
#14188=EDGE_CURVE ( 'NONE', #2684, #12318, #16923, .T. ) ;
#14239=CARTESIAN_POINT ( 'NONE',  ( 12.69999999999999929, -3653.789999999999964, 2262.355140000000119 ) ) ;
#14259=CARTESIAN_POINT ( 'NONE',  ( 12.69997737250858982, -3642.347301253999831, 2279.817639304488239 ) ) ;
#14331=SHAPE_REPRESENTATION_RELATIONSHIP ( 'NONE' , 'NONE' ,  #13400, #9094 ) ;
#14397=EDGE_CURVE ( 'NONE', #957, #17884, #7322, .T. ) ;
#14479=VECTOR ( 'NONE', #16092, 1000.000000000000000 ) ;
#14493=DIRECTION ( 'NONE',  ( 0.000000000000000000, 0.000000000000000000, -1.000000000000000000 ) ) ;
#14519=ORIENTED_EDGE ( 'NONE', *, *, #9247, .F. ) ;
#14561=CARTESIAN_POINT ( 'NONE',  ( 10.28172140950000113, -3641.012291280000227, 2279.551786969999739 ) ) ;
#14577=CARTESIAN_POINT ( 'NONE',  ( 12.69999999999999929, -3648.710000000000036, 2268.705139999999574 ) ) ;
#14651=CARTESIAN_POINT ( 'NONE',  ( 14.93205397128999934, -3641.276132144000258, 2279.591813953999463 ) ) ;
#14685=EDGE_CURVE ( 'NONE', #819, #20355, #2682, .T. ) ;
#14704=CIRCLE ( 'NONE', #22175, 2.844799999999999773 ) ;
#14715=EDGE_CURVE ( 'NONE', #12735, #3057, #11079, .T. ) ;
#14884=CARTESIAN_POINT ( 'NONE',  ( 14.21033034659000016, -3641.920435225999881, 2279.715679318999719 ) ) ;
#14950=DIRECTION ( 'NONE',  ( 0.000000000000000000, -1.000000000000000000, 0.000000000000000000 ) ) ;
#14990=CARTESIAN_POINT ( 'NONE',  ( 13.92840658401000020, -3642.075073558000440, 2279.750815596999928 ) ) ;
#15035=CARTESIAN_POINT ( 'NONE',  ( 12.69999999999999929, -3590.289999999999964, 2257.592639999999847 ) ) ;
#15089=ORIENTED_EDGE ( 'NONE', *, *, #17010, .F. ) ;
#15160=CIRCLE ( 'NONE', #2805, 11.11250000000000071 ) ;
#15176=FACE_OUTER_BOUND ( 'NONE', #4743, .T. ) ;
#15177=ADVANCED_FACE ( 'NONE', ( #4430 ), #2665, .T. ) ;
#15208=CARTESIAN_POINT ( 'NONE',  ( 9.855201422231997910, -3599.497499926000273, 2279.447341858000073 ) ) ;
#15230=CARTESIAN_POINT ( 'NONE',  ( 12.69999999999999929, -3590.289999999999964, 2268.705139999999574 ) ) ;
#15292=CARTESIAN_POINT ( 'NONE',  ( 10.12709285722000097, -3600.725217008999607, 2279.515989326000181 ) ) ;
#15306=DIRECTION ( 'NONE',  ( 0.000000000000000000, 0.000000000000000000, -1.000000000000000000 ) ) ;
#15392=CARTESIAN_POINT ( 'NONE',  ( 12.69999999999999929, -3653.027999999999793, 2274.293139999999767 ) ) ;
#15438=CARTESIAN_POINT ( 'NONE',  ( 12.07304487791000192, -3596.716615716000433, 2279.801384127999881 ) ) ;
#15496=CARTESIAN_POINT ( 'NONE',  ( 15.53321004273999861, -3599.811849713999891, 2279.450415087999772 ) ) ;
#15536=EDGE_CURVE ( 'NONE', #18172, #3458, #11541, .T. ) ;
#15552=CARTESIAN_POINT ( 'NONE',  ( 14.93205609083999974, -3637.728870509999979, 2279.591813517999981 ) ) ;
#15555=CARTESIAN_POINT ( 'NONE',  ( 10.68380249261999992, -3597.481841244999941, 2279.634034043999691 ) ) ;
#15558=ORIENTED_EDGE ( 'NONE', *, *, #21141, .F. ) ;
#15562=CARTESIAN_POINT ( 'NONE',  ( 12.70000000000085727, -3636.657698770567094, 2279.817639764978139 ) ) ;
#15610=ADVANCED_FACE ( 'NONE', ( #18585 ), #2535, .F. ) ;
#15618=ORIENTED_EDGE ( 'NONE', *, *, #18901, .T. ) ;
#15630=CYLINDRICAL_SURFACE ( 'NONE', #7061, 6.349999999999855760 ) ;
#15648=CARTESIAN_POINT ( 'NONE',  ( 12.69999999999999929, -3599.497499999999945, 2263.571799999999712 ) ) ;
#15713=EDGE_CURVE ( 'NONE', #819, #4457, #19165, .T. ) ;
#15848=CARTESIAN_POINT ( 'NONE',  ( 15.48106116729000092, -3600.123614707999877, 2279.464089926999804 ) ) ;
#15894=DIRECTION ( 'NONE',  ( 0.000000000000000000, -1.000000000000000000, 0.000000000000000000 ) ) ;
#15900=VERTEX_POINT ( 'NONE', #6265 ) ;
#15909=VERTEX_POINT ( 'NONE', #20208 ) ;
#15940=DIRECTION ( 'NONE',  ( 0.000000000000000000, 0.000000000000000000, 1.000000000000000000 ) ) ;
#15981=ORIENTED_EDGE ( 'NONE', *, *, #20739, .T. ) ;
#15994=DIRECTION ( 'NONE',  ( 0.000000000000000000, 0.000000000000000000, 1.000000000000000000 ) ) ;
#16059=LINE ( 'NONE', #6817, #22204 ) ;
#16084=VERTEX_POINT ( 'NONE', #20646 ) ;
#16092=DIRECTION ( 'NONE',  ( 0.000000000000000000, 0.000000000000000000, 1.000000000000000000 ) ) ;
#16107=DIRECTION ( 'NONE',  ( 0.000000000000000000, 1.000000000000000000, 0.000000000000000000 ) ) ;
#16185=AXIS2_PLACEMENT_3D ( 'NONE', #9233, #6404, #15306 ) ;
#16195=CARTESIAN_POINT ( 'NONE',  ( 10.68406120964000117, -3641.518414594000205, 2279.634081700000479 ) ) ;
#16240=ADVANCED_FACE ( 'NONE', ( #3426, #10580 ), #17716, .F. ) ;
#16244=CARTESIAN_POINT ( 'NONE',  ( 15.54479999999999862, -3599.497499999999945, 2279.447335734999797 ) ) ;
#16271=CARTESIAN_POINT ( 'NONE',  ( 10.68380249261999992, -3637.486841245000505, 2279.634034043999691 ) ) ;
#16361=CYLINDRICAL_SURFACE ( 'NONE', #3905, 2.844799999999999773 ) ;
#16479=ORIENTED_EDGE ( 'NONE', *, *, #20679, .F. ) ;
#16574=CARTESIAN_POINT ( 'NONE',  ( 12.70000000000000462, -3596.652698770568804, 2279.817639764978139 ) ) ;
#16582=FACE_OUTER_BOUND ( 'NONE', #4870, .T. ) ;
#16622=CIRCLE ( 'NONE', #12520, 5.587999999999926359 ) ;
#16632=CARTESIAN_POINT ( 'NONE',  ( 14.47434230490000040, -3597.266017030000057, 2279.676071933000003 ) ) ;
#16678=ADVANCED_FACE ( 'NONE', ( #10985 ), #1970, .T. ) ;
#16690=CARTESIAN_POINT ( 'NONE',  ( 12.69999261052944028, -3596.652698770683855, 2279.817639764992691 ) ) ;
#16715=ORIENTED_EDGE ( 'NONE', *, *, #10653, .F. ) ;
#16735=EDGE_CURVE ( 'NONE', #3057, #21632, #13311, .T. ) ;
#16741=UNCERTAINTY_MEASURE_WITH_UNIT (LENGTH_MEASURE( 1.000000000000000082E-05 ), #21126, 'distance_accuracy_value', 'NONE');
#16755=ORIENTED_EDGE ( 'NONE', *, *, #367, .F. ) ;
#16818=CARTESIAN_POINT ( 'NONE',  ( 12.70000000000000107, -3590.289999999999964, 2279.817639999999756 ) ) ;
#16890=DIRECTION ( 'NONE',  ( 0.000000000000000000, -1.000000000000000000, 0.000000000000000000 ) ) ;
#16891=ORIENTED_EDGE ( 'NONE', *, *, #18884, .F. ) ;
#16905=CARTESIAN_POINT ( 'NONE',  ( 12.69999999999999929, -3653.027999999999793, 2262.355140000000119 ) ) ;
#16908=B_SPLINE_CURVE_WITH_KNOTS ( 'NONE', 3,
 ( #10400, #19075, #8540, #15562 ),
 .UNSPECIFIED., .F., .F.,
 ( 4, 4 ),
 ( 0.000000000000000000, 5.006989800018624494E-06 ),
 .UNSPECIFIED. ) ;
#16920=CARTESIAN_POINT ( 'NONE',  ( 12.59469521408999881, -3602.342298742000366, 2279.817638609000369 ) ) ;
#16923=CIRCLE ( 'NONE', #19941, 2.844799999999999773 ) ;
#17001=EDGE_LOOP ( 'NONE', ( #3373, #22849 ) ) ;
#17010=EDGE_CURVE ( 'NONE', #7174, #1860, #14704, .T. ) ;
#17013=( LENGTH_UNIT ( ) NAMED_UNIT ( * ) SI_UNIT ( .MILLI., .METRE. ) );
#17031=VERTEX_POINT ( 'NONE', #7787 ) ;
#17040=DIRECTION ( 'NONE',  ( 0.000000000000000000, 0.000000000000000000, 1.000000000000000000 ) ) ;
#17044=VERTEX_POINT ( 'NONE', #16905 ) ;
#17063=CARTESIAN_POINT ( 'NONE',  ( 13.63269713621999912, -3636.808664902999681, 2279.779803621000156 ) ) ;
#17096=ORIENTED_EDGE ( 'NONE', *, *, #18084, .T. ) ;
#17100=ADVANCED_FACE ( 'NONE', ( #11624 ), #6146, .F. ) ;
#17147=EDGE_CURVE ( 'NONE', #17031, #18172, #9815, .T. ) ;
#17153=CARTESIAN_POINT ( 'NONE',  ( 12.69999999999999929, -3639.502500000000055, 2263.571799999999712 ) ) ;
#17245=CARTESIAN_POINT ( 'NONE',  ( 14.93205397128999934, -3601.271132144000148, 2279.591813953999463 ) ) ;
#17291=VERTEX_POINT ( 'NONE', #9630 ) ;
#17299=CARTESIAN_POINT ( 'NONE',  ( 9.866773677518999364, -3599.183293980000144, 2279.450408114000311 ) ) ;
#17328=VERTEX_POINT ( 'NONE', #11603 ) ;
#17332=VERTEX_POINT ( 'NONE', #18755 ) ;
#17455=ORIENTED_EDGE ( 'NONE', *, *, #7636, .F. ) ;
#17538=DIRECTION ( 'NONE',  ( 0.000000000000000000, 0.000000000000000000, -1.000000000000000000 ) ) ;
#17586=ORIENTED_EDGE ( 'NONE', *, *, #19156, .F. ) ;
#17630=CARTESIAN_POINT ( 'NONE',  ( 12.70000000000000107, -3590.289999999999964, 2279.817639999999756 ) ) ;
#17688=CIRCLE ( 'NONE', #5359, 11.11250000000000071 ) ;
#17699=ORIENTED_EDGE ( 'NONE', *, *, #20969, .F. ) ;
#17701=DIRECTION ( 'NONE',  ( 0.000000000000000000, -1.000000000000000000, 0.000000000000000000 ) ) ;
#17716=PLANE ( 'NONE',  #18784 ) ;
#17740=DIRECTION ( 'NONE',  ( 0.000000000000000000, -1.000000000000000000, 0.000000000000000000 ) ) ;
#17788=DIRECTION ( 'NONE',  ( 0.000000000000000000, -1.000000000000000000, 0.000000000000000000 ) ) ;
#17796=ORIENTED_EDGE ( 'NONE', *, *, #5241, .T. ) ;
#17882=CARTESIAN_POINT ( 'NONE',  ( 12.69999999999999929, -3648.710000000000036, 2275.055139999999483 ) ) ;
#17884=VERTEX_POINT ( 'NONE', #19989 ) ;
#17940=CARTESIAN_POINT ( 'NONE',  ( 12.69999999999999929, -3653.789999999999964, 2263.117139999999836 ) ) ;
#18065=CARTESIAN_POINT ( 'NONE',  ( 9.855201422231997910, -3639.502499925999928, 2279.447341858000073 ) ) ;
#18074=AXIS2_PLACEMENT_3D ( 'NONE', #13167, #21958, #2727 ) ;
#18084=EDGE_CURVE ( 'NONE', #12318, #2684, #13607, .T. ) ;
#18117=EDGE_CURVE ( 'NONE', #1860, #7174, #10998, .T. ) ;
#18134=AXIS2_PLACEMENT_3D ( 'NONE', #1355, #5120, #8520 ) ;
#18137=CARTESIAN_POINT ( 'NONE',  ( 12.07304487791000192, -3636.721615716000088, 2279.801384127999881 ) ) ;
#18156=EDGE_CURVE ( 'NONE', #2684, #20725, #16059, .T. ) ;
#18167=CARTESIAN_POINT ( 'NONE',  ( 14.21033367406000103, -3597.079566860000341, 2279.715678855999613 ) ) ;
#18172=VERTEX_POINT ( 'NONE', #13843 ) ;
#18202=ORIENTED_EDGE ( 'NONE', *, *, #14715, .F. ) ;
#18230=CARTESIAN_POINT ( 'NONE',  ( 12.69999999999999929, -3639.502500000000055, 2263.571799999999712 ) ) ;
#18290=AXIS2_PLACEMENT_3D ( 'NONE', #21500, #12416, #231 ) ;
#18291=VERTEX_POINT ( 'NONE', #1526 ) ;
#18292=CARTESIAN_POINT ( 'NONE',  ( 9.855199999999999960, -3599.497499999999945, 2263.571799999999712 ) ) ;
#18322=CIRCLE ( 'NONE', #10081, 6.349999999999855760 ) ;
#18329=DIRECTION ( 'NONE',  ( 0.000000000000000000, 0.000000000000000000, 1.000000000000000000 ) ) ;
#18340=EDGE_LOOP ( 'NONE', ( #16715, #11172, #19527, #16891 ) ) ;
#18396=CARTESIAN_POINT ( 'NONE',  ( 13.01510790209939827, -3596.664354860411095, 2279.814648369741462 ) ) ;
#18439=EDGE_CURVE ( 'NONE', #17884, #20138, #12874, .T. ) ;
#18481=VERTEX_POINT ( 'NONE', #1386 ) ;
#18485=ORIENTED_EDGE ( 'NONE', *, *, #4149, .T. ) ;
#18490=B_SPLINE_CURVE_WITH_KNOTS ( 'NONE', 3,
 ( #1891, #21591, #5547, #21357, #26, #19595, #9044, #12561, #16195, #12677, #14561, #3758, #3883, #21814, #10915, #3529, #18065 ),
 .UNSPECIFIED., .F., .F.,
 ( 4, 1, 1, 1, 1, 1, 1, 1, 1, 1, 1, 1, 1, 1, 4 ),
 ( 0.000000000000000000, 0.07142857142856999519, 0.1428571428570999946, 0.2142857142857000075, 0.2857142857143000203, 0.3571428571429000054, 0.4285714285713999594, 0.5000000000000000000, 0.5714285714286000406, 0.6428571428570999391, 0.7142857142856999797, 0.7857142857142999093, 0.8571428571429000609, 0.9285714285714000704, 1.000000000000000000 ),
 .UNSPECIFIED. ) ;
#18497=CARTESIAN_POINT ( 'NONE',  ( 15.53321004273999861, -3639.816849713999545, 2279.450415087999772 ) ) ;
#18511=CARTESIAN_POINT ( 'NONE',  ( 13.92841025336000094, -3596.924928188000194, 2279.750815200000034 ) ) ;
#18541=EDGE_LOOP ( 'NONE', ( #20857, #7085, #21489, #256 ) ) ;
#18585=FACE_OUTER_BOUND ( 'NONE', #20188, .T. ) ;
#18604=CARTESIAN_POINT ( 'NONE',  ( 9.855199999999999960, -3639.502500000000055, 2263.571799999999712 ) ) ;
#18642=CARTESIAN_POINT ( 'NONE',  ( 12.69998491500983206, -3602.342301254179802, 2279.817638609000369 ) ) ;
#18643=B_SPLINE_CURVE_WITH_KNOTS ( 'NONE', 3,
 ( #20698, #13558, #11796, #11916, #17063, #2771, #19064, #9803, #6192, #15552, #9694, #20580, #6539, #18948, #9914, #8287, #20827 ),
 .UNSPECIFIED., .F., .F.,
 ( 4, 1, 1, 1, 1, 1, 1, 1, 1, 1, 1, 1, 1, 1, 4 ),
 ( 5.006989800018624494E-06, 0.07142857142856999519, 0.1428571428570999946, 0.2142857142857000075, 0.2857142857143000203, 0.3571428571429000054, 0.4285714285713999594, 0.5000000000000000000, 0.5714285714286000406, 0.6428571428570999391, 0.7142857142856999797, 0.7857142857142999093, 0.8571428571429000609, 0.9285714285714000704, 1.000000000000000000 ),
 .UNSPECIFIED. ) ;
#18682=CARTESIAN_POINT ( 'NONE',  ( 9.855201422231997910, -3599.602849033000439, 2279.447341858000073 ) ) ;
#18715=CARTESIAN_POINT ( 'NONE',  ( 12.69999999999999929, -3599.497499999999945, 2263.571799999999712 ) ) ;
#18755=CARTESIAN_POINT ( 'NONE',  ( 15.54479999999999862, -3639.502500000000055, 2279.447335734999797 ) ) ;
#18784=AXIS2_PLACEMENT_3D ( 'NONE', #5427, #1666, #8822 ) ;
#18797=CARTESIAN_POINT ( 'NONE',  ( 12.69997737251000025, -3602.342301254000176, 2279.817638609000369 ) ) ;
#18852=DIRECTION ( 'NONE',  ( 0.000000000000000000, -1.000000000000000000, 0.000000000000000000 ) ) ;
#18875=ADVANCED_FACE ( 'NONE', ( #21170 ), #21137, .T. ) ;
#18881=ORIENTED_EDGE ( 'NONE', *, *, #18084, .F. ) ;
#18884=EDGE_CURVE ( 'NONE', #17328, #3458, #22606, .T. ) ;
#18891=DIRECTION ( 'NONE',  ( 0.000000000000000000, -1.000000000000000000, 0.000000000000000000 ) ) ;
#18901=EDGE_CURVE ( 'NONE', #17031, #2645, #16622, .T. ) ;
#18936=TOROIDAL_SURFACE ( 'NONE', #8845, 5.588000000000000078, 0.7620000000000000107 ) ;
#18948=CARTESIAN_POINT ( 'NONE',  ( 15.48106175502000070, -3638.876388315999975, 2279.464089773000069 ) ) ;
#18963=AXIS2_PLACEMENT_3D ( 'NONE', #1798, #13989, #22872 ) ;
#18969=DIRECTION ( 'NONE',  ( 0.000000000000000000, 1.000000000000000000, 0.000000000000000000 ) ) ;
#19064=CARTESIAN_POINT ( 'NONE',  ( 14.21033367406000103, -3637.084566859999995, 2279.715678855999613 ) ) ;
#19075=CARTESIAN_POINT ( 'NONE',  ( 12.69998522105638905, -3636.657698770827210, 2279.817639764999967 ) ) ;
#19104=ORIENTED_EDGE ( 'NONE', *, *, #18156, .T. ) ;
#19127=ORIENTED_EDGE ( 'NONE', *, *, #4149, .F. ) ;
#19131=CARTESIAN_POINT ( 'NONE',  ( 15.11851036462000053, -3601.006922181999926, 2279.551735152999754 ) ) ;
#19154=EDGE_CURVE ( 'NONE', #16084, #5789, #10907, .T. ) ;
#19156=EDGE_CURVE ( 'NONE', #18481, #4457, #15160, .T. ) ;
#19165=LINE ( 'NONE', #17630, #8665 ) ;
#19289=ORIENTED_EDGE ( 'NONE', *, *, #3814, .T. ) ;
#19382=DIRECTION ( 'NONE',  ( 0.000000000000000000, 0.000000000000000000, -1.000000000000000000 ) ) ;
#19527=ORIENTED_EDGE ( 'NONE', *, *, #15536, .T. ) ;
#19540=CARTESIAN_POINT ( 'NONE',  ( 12.69999999999999929, -3585.971999999999753, 2268.705139999999574 ) ) ;
#19595=CARTESIAN_POINT ( 'NONE',  ( 11.47192027633000144, -3642.075229274999856, 2279.750852048000070 ) ) ;
#19605=DIRECTION ( 'NONE',  ( 0.000000000000000000, -1.000000000000000000, 0.000000000000000000 ) ) ;
#19663=CARTESIAN_POINT ( 'NONE',  ( 12.70000000000000107, -3590.289999999999964, 2279.817639999999756 ) ) ;
#19674=CARTESIAN_POINT ( 'NONE',  ( 12.69999999999999929, -3585.210000000000036, 2263.117139999999836 ) ) ;
#19695=ADVANCED_FACE ( 'NONE', ( #9716 ), #8195, .T. ) ;
#19766=CARTESIAN_POINT ( 'NONE',  ( 12.69999999999999929, -3585.210000000000036, 2268.705139999999574 ) ) ;
#19774=CARTESIAN_POINT ( 'NONE',  ( 12.70000000000085727, -3636.657698770567094, 2279.817639764978139 ) ) ;
#19787=LINE ( 'NONE', #19663, #4031 ) ;
#19798=ORIENTED_EDGE ( 'NONE', *, *, #11880, .T. ) ;
#19839=ORIENTED_EDGE ( 'NONE', *, *, #4360, .F. ) ;
#19917=ORIENTED_EDGE ( 'NONE', *, *, #19156, .T. ) ;
#19941=AXIS2_PLACEMENT_3D ( 'NONE', #14127, #15994, #23008 ) ;
#19962=CLOSED_SHELL ( 'NONE', ( #1066, #10525, #19695, #9164, #17100, #5837, #6679, #15610, #12890, #3550, #18875, #21762, #10795, #13001, #12843, #21879, #15177, #16240, #16678, #9661 ) ) ;
#19989=CARTESIAN_POINT ( 'NONE',  ( 12.69999999999999929, -3590.289999999999964, 2262.355140000000119 ) ) ;
#20000=ORIENTED_EDGE ( 'NONE', *, *, #19154, .F. ) ;
#20054=VECTOR ( 'NONE', #6077, 1000.000000000000000 ) ;
#20057=EDGE_CURVE ( 'NONE', #15900, #8731, #8083, .T. ) ;
#20062=CARTESIAN_POINT ( 'NONE',  ( 9.918918857905000053, -3598.871466521999537, 2279.464085466000142 ) ) ;
#20070=CARTESIAN_POINT ( 'NONE',  ( 12.69997783158000004, -3636.657698770999559, 2279.817639764999967 ) ) ;
#20072=DIRECTION ( 'NONE',  ( 0.000000000000000000, 0.000000000000000000, -1.000000000000000000 ) ) ;
#20138=VERTEX_POINT ( 'NONE', #4308 ) ;
#20153=ORIENTED_EDGE ( 'NONE', *, *, #21334, .T. ) ;
#20163=ORIENTED_EDGE ( 'NONE', *, *, #7578, .T. ) ;
#20188=EDGE_LOOP ( 'NONE', ( #12463, #17796 ) ) ;
#20201=CARTESIAN_POINT ( 'NONE',  ( 12.69999999999999929, -3648.710000000000036, 2268.705139999999574 ) ) ;
#20208=CARTESIAN_POINT ( 'NONE',  ( 12.69997737251000025, -3602.342301254000176, 2279.817638609000369 ) ) ;
#20261=UNCERTAINTY_MEASURE_WITH_UNIT (LENGTH_MEASURE( 1.000000000000000082E-05 ), #17013, 'distance_accuracy_value', 'NONE');
#20277=EDGE_LOOP ( 'NONE', ( #17096, #11829 ) ) ;
#20302=ORIENTED_EDGE ( 'NONE', *, *, #17147, .T. ) ;
#20316=FACE_OUTER_BOUND ( 'NONE', #9085, .T. ) ;
#20355=VERTEX_POINT ( 'NONE', #14259 ) ;
#20431=CARTESIAN_POINT ( 'NONE',  ( 12.69999999999999929, -3639.502500000000055, 2263.571799999999712 ) ) ;
#20449=CARTESIAN_POINT ( 'NONE',  ( 11.76763247656000111, -3602.191447740999592, 2279.779831143999672 ) ) ;
#20559=CARTESIAN_POINT ( 'NONE',  ( 12.69999999999999929, -3653.789999999999964, 2275.055139999999483 ) ) ;
#20561=CIRCLE ( 'NONE', #4474, 0.7619999999999294005 ) ;
#20572=EDGE_LOOP ( 'NONE', ( #16479, #9410, #9632, #16755 ) ) ;
#20580=CARTESIAN_POINT ( 'NONE',  ( 15.27310946263999902, -3638.275206607999735, 2279.515940941999816 ) ) ;
#20646=CARTESIAN_POINT ( 'NONE',  ( 12.69997932225824400, -3596.652698770999905, 2279.817639835496266 ) ) ;
#20667=DIRECTION ( 'NONE',  ( 0.000000000000000000, 0.000000000000000000, 1.000000000000000000 ) ) ;
#20679=EDGE_CURVE ( 'NONE', #17291, #20138, #6971, .T. ) ;
#20683=EDGE_CURVE ( 'NONE', #2780, #17291, #8476, .T. ) ;
#20698=CARTESIAN_POINT ( 'NONE',  ( 12.70000000000085727, -3636.657698770567094, 2279.817639764978139 ) ) ;
#20712=AXIS2_PLACEMENT_3D ( 'NONE', #1648, #17701, #8806 ) ;
#20725=VERTEX_POINT ( 'NONE', #2159 ) ;
#20739=EDGE_CURVE ( 'NONE', #4457, #18481, #8421, .T. ) ;
#20751=ORIENTED_EDGE ( 'NONE', *, *, #13868, .F. ) ;
#20761=AXIS2_PLACEMENT_3D ( 'NONE', #17153, #13071, #14950 ) ;
#20768=CARTESIAN_POINT ( 'NONE',  ( 13.01510455369341557, -3602.330645362285395, 2279.814648973302610 ) ) ;
#20790=DIRECTION ( 'NONE',  ( 1.000000000000000000, 0.000000000000000000, 0.000000000000000000 ) ) ;
#20812=VECTOR ( 'NONE', #4735, 1000.000000000000000 ) ;
#20827=CARTESIAN_POINT ( 'NONE',  ( 15.54479999999999862, -3639.502500000000055, 2279.447335734999797 ) ) ;
#20829=CARTESIAN_POINT ( 'NONE',  ( 10.92571717110000051, -3597.265967912000178, 2279.676081828000406 ) ) ;
#20843=DIRECTION ( 'NONE',  ( 0.000000000000000000, 0.000000000000000000, 1.000000000000000000 ) ) ;
#20857=ORIENTED_EDGE ( 'NONE', *, *, #22964, .F. ) ;
#20883=AXIS2_PLACEMENT_3D ( 'NONE', #19540, #1963, #10981 ) ;
#20884=LINE ( 'NONE', #12087, #925 ) ;
#20890=ORIENTED_EDGE ( 'NONE', *, *, #22964, .T. ) ;
#20894=CARTESIAN_POINT ( 'NONE',  ( 15.39424449907000003, -3600.429004351000003, 2279.486256451000372 ) ) ;
#20910=ORIENTED_EDGE ( 'NONE', *, *, #21311, .F. ) ;
#20932=DIRECTION ( 'NONE',  ( 0.000000000000000000, 0.000000000000000000, -1.000000000000000000 ) ) ;
#20948=CARTESIAN_POINT ( 'NONE',  ( 12.69999999999999929, -3590.289999999999964, 2268.705139999999574 ) ) ;
#20969=EDGE_CURVE ( 'NONE', #22051, #18481, #21942, .T. ) ;
#21042=ORIENTED_EDGE ( 'NONE', *, *, #9247, .T. ) ;
#21043=DIRECTION ( 'NONE',  ( 0.000000000000000000, 0.000000000000000000, -1.000000000000000000 ) ) ;
#21047=ORIENTED_EDGE ( 'NONE', *, *, #5936, .T. ) ;
#21126=( LENGTH_UNIT ( ) NAMED_UNIT ( * ) SI_UNIT ( .MILLI., .METRE. ) );
#21133=CARTESIAN_POINT ( 'NONE',  ( 12.69999999999999929, -3585.210000000000036, 2268.705139999999574 ) ) ;
#21137=TOROIDAL_SURFACE ( 'NONE', #18134, 5.588000000000000078, 0.7620000000000000107 ) ;
#21141=EDGE_CURVE ( 'NONE', #7174, #17332, #20884, .T. ) ;
#21154=FACE_OUTER_BOUND ( 'NONE', #192, .T. ) ;
#21162=APPLICATION_CONTEXT ( 'configuration controlled 3d designs of mechanical parts and assemblies' ) ;
#21170=FACE_OUTER_BOUND ( 'NONE', #6528, .T. ) ;
#21212=VECTOR ( 'NONE', #16107, 1000.000000000000000 ) ;
#21311=EDGE_CURVE ( 'NONE', #1860, #15900, #7594, .T. ) ;
#21334=EDGE_CURVE ( 'NONE', #21632, #17332, #18643, .T. ) ;
#21357=CARTESIAN_POINT ( 'NONE',  ( 12.07314413848000001, -3642.283404631000394, 2279.801389126999766 ) ) ;
#21417=EDGE_LOOP ( 'NONE', ( #1021, #18881, #88, #7828, #20000, #20751 ) ) ;
#21489=ORIENTED_EDGE ( 'NONE', *, *, #18439, .F. ) ;
#21492=AXIS2_PLACEMENT_3D ( 'NONE', #10527, #17788, #3372 ) ;
#21500=CARTESIAN_POINT ( 'NONE',  ( 12.69999999999999929, -3653.027999999999793, 2268.705139999999574 ) ) ;
#21544=VECTOR ( 'NONE', #16890, 1000.000000000000000 ) ;
#21547=AXIS2_PLACEMENT_3D ( 'NONE', #3524, #1781, #23 ) ;
#21551=CARTESIAN_POINT ( 'NONE',  ( 9.855201422231997910, -3639.502499925999928, 2279.447341858000073 ) ) ;
#21583=CARTESIAN_POINT ( 'NONE',  ( 15.54479999999999862, -3599.392331916999865, 2279.447335734999797 ) ) ;
#21591=CARTESIAN_POINT ( 'NONE',  ( 12.59469521408999881, -3642.347298742000021, 2279.817638609000369 ) ) ;
#21632=VERTEX_POINT ( 'NONE', #19774 ) ;
#21688=ORIENTED_EDGE ( 'NONE', *, *, #18117, .F. ) ;
#21719=DIRECTION ( 'NONE',  ( 0.000000000000000000, -1.000000000000000000, 0.000000000000000000 ) ) ;
#21744=DIRECTION ( 'NONE',  ( 1.000000000000000000, 0.000000000000000000, 0.000000000000000000 ) ) ;
#21751=CYLINDRICAL_SURFACE ( 'NONE', #4356, 6.349999999999855760 ) ;
#21762=ADVANCED_FACE ( 'NONE', ( #9555 ), #21751, .T. ) ;
#21803=CARTESIAN_POINT ( 'NONE',  ( 14.93205609083999974, -3597.723870509999870, 2279.591813517999981 ) ) ;
#21813=DIRECTION ( 'NONE',  ( 0.000000000000000000, 1.000000000000000000, 0.000000000000000000 ) ) ;
#21814=CARTESIAN_POINT ( 'NONE',  ( 9.919062418924999847, -3640.129156706999765, 2279.464122714000041 ) ) ;
#21836=DIRECTION ( 'NONE',  ( 1.000000000000000000, 0.000000000000000000, 3.996303350731721563E-14 ) ) ;
#21850=EDGE_CURVE ( 'NONE', #15909, #20725, #8604, .T. ) ;
#21879=ADVANCED_FACE ( 'NONE', ( #9775 ), #8150, .F. ) ;
#21890=CARTESIAN_POINT ( 'NONE',  ( 15.54479999999999862, -3599.497499999999945, 2263.571799999999712 ) ) ;
#21942=LINE ( 'NONE', #15035, #21544 ) ;
#21958=DIRECTION ( 'NONE',  ( 0.000000000000000000, 0.000000000000000000, 1.000000000000000000 ) ) ;
#22013=CARTESIAN_POINT ( 'NONE',  ( 14.47433926966999884, -3641.733985386000313, 2279.676072425999791 ) ) ;
#22024=CARTESIAN_POINT ( 'NONE',  ( 15.53320999718999929, -3599.183150532000127, 2279.450415100000100 ) ) ;
#22051=VERTEX_POINT ( 'NONE', #13882 ) ;
#22158=EDGE_CURVE ( 'NONE', #17044, #18172, #22387, .T. ) ;
#22175=AXIS2_PLACEMENT_3D ( 'NONE', #20431, #18329, #853 ) ;
#22204=VECTOR ( 'NONE', #13956, 1000.000000000000000 ) ;
#22317=DIRECTION ( 'NONE',  ( 0.000000000000000000, 1.000000000000000000, 0.000000000000000000 ) ) ;
#22361=EDGE_LOOP ( 'NONE', ( #2081, #12941 ) ) ;
#22387=CIRCLE ( 'NONE', #18290, 6.349999999999855760 ) ;
#22392=CARTESIAN_POINT ( 'NONE',  ( 12.69999999999999929, -3585.210000000000036, 2268.705139999999574 ) ) ;
#22423=CARTESIAN_POINT ( 'NONE',  ( 12.69999999999999929, -3639.502500000000055, 2263.571799999999712 ) ) ;
#22449=CARTESIAN_POINT ( 'NONE',  ( 12.59468037889999970, -3596.652701232999789, 2279.817639764999967 ) ) ;
#22467=FACE_OUTER_BOUND ( 'NONE', #4252, .T. ) ;
#22505=ORIENTED_EDGE ( 'NONE', *, *, #3490, .F. ) ;
#22521=DIRECTION ( 'NONE',  ( -1.000000000000000000, 0.000000000000000000, 0.000000000000000000 ) ) ;
#22537=CARTESIAN_POINT ( 'NONE',  ( 12.07314413848000001, -3602.278404630999830, 2279.801389126999766 ) ) ;
#22538=EDGE_LOOP ( 'NONE', ( #10028, #22505, #18485, #4757 ) ) ;
#22573=AXIS2_PLACEMENT_3D ( 'NONE', #22423, #6396, #10018 ) ;
#22606=CIRCLE ( 'NONE', #8033, 6.349999999999855760 ) ;
#22698=ORIENTED_EDGE ( 'NONE', *, *, #20969, .T. ) ;
#22787=CARTESIAN_POINT ( 'NONE',  ( 12.69999999999999929, -3648.710000000000036, 2268.705139999999574 ) ) ;
#22796=PRODUCT_DEFINITION ( 'UNKNOWN', '', #2608, #10183 ) ;
#22849=ORIENTED_EDGE ( 'NONE', *, *, #18884, .T. ) ;
#22872=DIRECTION ( 'NONE',  ( 0.000000000000000000, 0.000000000000000000, 1.000000000000000000 ) ) ;
#22964=EDGE_CURVE ( 'NONE', #17291, #957, #18322, .T. ) ;
#22979=CARTESIAN_POINT ( 'NONE',  ( 14.71622237244000075, -3601.513131979999798, 2279.634029254999859 ) ) ;
#23008=DIRECTION ( 'NONE',  ( -1.000000000000000000, 0.000000000000000000, 0.000000000000000000 ) ) ;
#23082=ORIENTED_EDGE ( 'NONE', *, *, #22158, .F. ) ;
#23094=( NAMED_UNIT ( * ) SI_UNIT ( $, .STERADIAN. ) SOLID_ANGLE_UNIT ( ) );
#23215=COLOUR_RGB('Off White',0.89,0.88,0.83);
#23216=FILL_AREA_STYLE_COLOUR('',#23215);
#23217=FILL_AREA_STYLE('',(#23216));
#23218=SURFACE_STYLE_FILL_AREA(#23217);
#23219=SURFACE_SIDE_STYLE('',(#23218));
#23220=SURFACE_STYLE_USAGE(.BOTH.,#23219);
#23221=PRESENTATION_STYLE_ASSIGNMENT((#23220));
#23229=STYLED_ITEM('',(#23221),#6209);
#23237=MECHANICAL_DESIGN_GEOMETRIC_PRESENTATION_REPRESENTATION('',(#23229),#2257);
ENDSEC;
END-ISO-10303-21;
